ISO-10303-21;
HEADER;
FILE_DESCRIPTION (('STEP AP214'),
    '1' );
FILE_NAME ('1.4 Collar.step',
    '2026-10-06T08:51:13',
    ( '' ),
    ( '' ),
    'SwSTEP 2.0',
    'SolidWorks 2021',
    '' );
FILE_SCHEMA (( 'AUTOMOTIVE_DESIGN' ));
ENDSEC;

DATA;
#33=CARTESIAN_POINT ( 'NONE',  ( -1.180000000000000604, 10.00000000000000178, 6.750000000000000888 ) ) ;
#195=FACE_OUTER_BOUND ( 'NONE', #108561, .T. ) ;
#838=SURFACE_STYLE_FILL_AREA ( #111022 ) ;
#1108=FACE_OUTER_BOUND ( 'NONE', #128603, .T. ) ;
#2038=CIRCLE ( 'NONE', #87666, 9.119999999999999218 ) ;
#2069=ORIENTED_EDGE ( 'NONE', *, *, #32465, .F. ) ;
#2483=AXIS2_PLACEMENT_3D ( 'NONE', #94497, #59080, #82936 ) ;
#2640=CARTESIAN_POINT ( 'NONE',  ( -9.119999999999999218, 0.000000000000000000, 10.00000000000000000 ) ) ;
#2670=ORIENTED_EDGE ( 'NONE', *, *, #114502, .T. ) ;
#2858=ORIENTED_EDGE ( 'NONE', *, *, #35205, .F. ) ;
#3011=ORIENTED_EDGE ( 'NONE', *, *, #104011, .T. ) ;
#3077=ORIENTED_EDGE ( 'NONE', *, *, #6967, .T. ) ;
#3100=VECTOR ( 'NONE', #123808, 1000.000000000000000 ) ;
#3201=ORIENTED_EDGE ( 'NONE', *, *, #79876, .F. ) ;
#3582=VECTOR ( 'NONE', #36358, 1000.000000000000000 ) ;
#3693=EDGE_CURVE ( 'NONE', #133079, #18391, #101151, .T. ) ;
#3722=CARTESIAN_POINT ( 'NONE',  ( -1.179999999999997939, -9.043340090917734386, 10.00000000000000000 ) ) ;
#4621=CLOSED_SHELL ( 'NONE', ( #52502, #91665, #52315, #13962, #78021, #75969, #134383, #125716, #55019, #90440, #104262, #68389, #21319 ) ) ;
#4836=DIRECTION ( 'NONE',  ( -0.000000000000000000, -0.000000000000000000, -1.000000000000000000 ) ) ;
#5158=LINE ( 'NONE', #3722, #125018 ) ;
#5198=MECHANICAL_DESIGN_GEOMETRIC_PRESENTATION_REPRESENTATION('',(#44598),#81624);
#5945=VERTEX_POINT ( 'NONE', #24536 ) ;
#6232=VECTOR ( 'NONE', #111125, 1000.000000000000000 ) ;
#6967=EDGE_CURVE ( 'NONE', #19931, #42357, #58876, .T. ) ;
#6981=EDGE_CURVE ( 'NONE', #35420, #42357, #10618, .T. ) ;
#7493=DIRECTION ( 'NONE',  ( 1.000000000000000000, 0.000000000000000000, 0.000000000000000000 ) ) ;
#7749=DIRECTION ( 'NONE',  ( 1.000000000000000000, 0.000000000000000000, 0.000000000000000000 ) ) ;
#7796=EDGE_CURVE ( 'NONE', #62812, #81522, #51754, .T. ) ;
#8041=ORIENTED_EDGE ( 'NONE', *, *, #47807, .F. ) ;
#8111=EDGE_LOOP ( 'NONE', ( #34052, #2670, #17268, #15931, #101188, #18714, #75186, #125162 ) ) ;
#8492=DIRECTION ( 'NONE',  ( -1.084202172485504434E-16, 1.000000000000000000, -0.000000000000000000 ) ) ;
#8715=DIRECTION ( 'NONE',  ( 0.000000000000000000, 0.000000000000000000, 1.000000000000000000 ) ) ;
#8925=CARTESIAN_POINT ( 'NONE',  ( 0.000000000000000000, 0.000000000000000000, 0.000000000000000000 ) ) ;
#9142=AXIS2_PLACEMENT_3D ( 'NONE', #69823, #99526, #113268 ) ;
#9869=LINE ( 'NONE', #88894, #86081 ) ;
#10065=FACE_OUTER_BOUND ( 'NONE', #143477, .T. ) ;
#10396=ORIENTED_EDGE ( 'NONE', *, *, #135348, .F. ) ;
#10618=CIRCLE ( 'NONE', #91673, 6.499999999999999112 ) ;
#10661=DIRECTION ( 'NONE',  ( -0.000000000000000000, -0.000000000000000000, -1.000000000000000000 ) ) ;
#10785=AXIS2_PLACEMENT_3D ( 'NONE', #127889, #106804, #7493 ) ;
#11735=AXIS2_PLACEMENT_3D ( 'NONE', #33, #45762, #25383 ) ;
#11899=DIRECTION ( 'NONE',  ( 0.000000000000000000, 0.000000000000000000, 1.000000000000000000 ) ) ;
#12850=PLANE ( 'NONE',  #17339 ) ;
#13502=EDGE_CURVE ( 'NONE', #18391, #66770, #124405, .T. ) ;
#13962=ADVANCED_FACE ( 'NONE', ( #1108 ), #101867, .T. ) ;
#14539=ORIENTED_EDGE ( 'NONE', *, *, #7796, .T. ) ;
#14719=CARTESIAN_POINT ( 'NONE',  ( 0.000000000000000000, 0.000000000000000000, 10.00000000000000000 ) ) ;
#14898=ORIENTED_EDGE ( 'NONE', *, *, #36665, .F. ) ;
#15280=VERTEX_POINT ( 'NONE', #35241 ) ;
#15387=DIRECTION ( 'NONE',  ( 1.192622389734054877E-16, -1.000000000000000000, 0.000000000000000000 ) ) ;
#15788=CARTESIAN_POINT ( 'NONE',  ( 1.180000000000000604, -6.391994993740214959, 10.00000000000000000 ) ) ;
#15931=ORIENTED_EDGE ( 'NONE', *, *, #102498, .T. ) ;
#15960=CARTESIAN_POINT ( 'NONE',  ( 1.179999999999999272, 10.00000000000000178, 6.750000000000000888 ) ) ;
#16018=ORIENTED_EDGE ( 'NONE', *, *, #7796, .F. ) ;
#17046=CARTESIAN_POINT ( 'NONE',  ( 0.000000000000000000, 0.000000000000000000, 10.00000000000000000 ) ) ;
#17165=CARTESIAN_POINT ( 'NONE',  ( 0.000000000000000000, 0.000000000000000000, 6.750000000000000888 ) ) ;
#17232=AXIS2_PLACEMENT_3D ( 'NONE', #92735, #49980, #94163 ) ;
#17268=ORIENTED_EDGE ( 'NONE', *, *, #54279, .F. ) ;
#17339=AXIS2_PLACEMENT_3D ( 'NONE', #78147, #89033, #99883 ) ;
#17661=AXIS2_PLACEMENT_3D ( 'NONE', #111453, #52774, #86866 ) ;
#17924=ORIENTED_EDGE ( 'NONE', *, *, #66583, .T. ) ;
#18309=DIRECTION ( 'NONE',  ( 1.000000000000000000, 0.000000000000000000, 0.000000000000000000 ) ) ;
#18391=VERTEX_POINT ( 'NONE', #110978 ) ;
#18714=ORIENTED_EDGE ( 'NONE', *, *, #90844, .T. ) ;
#19293=EDGE_LOOP ( 'NONE', ( #59158, #50522, #133619, #55623, #26521, #138751, #3201, #142303 ) ) ;
#19931=VERTEX_POINT ( 'NONE', #113716 ) ;
#20723=EDGE_CURVE ( 'NONE', #78949, #62812, #2038, .T. ) ;
#21081=EDGE_CURVE ( 'NONE', #42357, #35420, #106258, .T. ) ;
#21319=ADVANCED_FACE ( 'NONE', ( #10065 ), #43425, .T. ) ;
#21456=AXIS2_PLACEMENT_3D ( 'NONE', #132171, #21951, #32122 ) ;
#21673=DIRECTION ( 'NONE',  ( 1.000000000000000000, 0.000000000000000000, 0.000000000000000000 ) ) ;
#21951=DIRECTION ( 'NONE',  ( 0.000000000000000000, 0.000000000000000000, 1.000000000000000000 ) ) ;
#22168=EDGE_CURVE ( 'NONE', #41309, #81522, #5158, .T. ) ;
#22459=VERTEX_POINT ( 'NONE', #122505 ) ;
#22469=EDGE_CURVE ( 'NONE', #78949, #99639, #110197, .T. ) ;
#23021=DIRECTION ( 'NONE',  ( 0.000000000000000000, 0.000000000000000000, 1.000000000000000000 ) ) ;
#23490=ORIENTED_EDGE ( 'NONE', *, *, #127884, .T. ) ;
#24003=AXIS2_PLACEMENT_3D ( 'NONE', #17046, #70740, #38800 ) ;
#24212=( GEOMETRIC_REPRESENTATION_CONTEXT ( 3 ) GLOBAL_UNCERTAINTY_ASSIGNED_CONTEXT ( ( #124631 ) ) GLOBAL_UNIT_ASSIGNED_CONTEXT ( ( #79181, #98732, #134981 ) ) REPRESENTATION_CONTEXT ( 'NONE', 'WORKASPACE' ) );
#24481=LINE ( 'NONE', #68732, #54957 ) ;
#24536=CARTESIAN_POINT ( 'NONE',  ( 1.179999999999999272, 9.043340090917736163, 6.750000000000000888 ) ) ;
#24645=VECTOR ( 'NONE', #38305, 1000.000000000000000 ) ;
#24863=DIRECTION ( 'NONE',  ( -1.000000000000000000, -1.192622389734054877E-16, 0.000000000000000000 ) ) ;
#25184=CARTESIAN_POINT ( 'NONE',  ( 0.000000000000000000, 0.000000000000000000, 10.00000000000000000 ) ) ;
#25383=DIRECTION ( 'NONE',  ( 1.192622389734054877E-16, -1.000000000000000000, 0.000000000000000000 ) ) ;
#26369=FACE_OUTER_BOUND ( 'NONE', #65871, .T. ) ;
#26521=ORIENTED_EDGE ( 'NONE', *, *, #20723, .F. ) ;
#26527=VERTEX_POINT ( 'NONE', #48440 ) ;
#27038=VERTEX_POINT ( 'NONE', #86449 ) ;
#27927=VERTEX_POINT ( 'NONE', #85353 ) ;
#28074=FACE_OUTER_BOUND ( 'NONE', #19293, .T. ) ;
#28973=EDGE_LOOP ( 'NONE', ( #136955, #58489, #56650, #14898 ) ) ;
#29700=ORIENTED_EDGE ( 'NONE', *, *, #42088, .F. ) ;
#30147=ORIENTED_EDGE ( 'NONE', *, *, #127884, .F. ) ;
#30594=ORIENTED_EDGE ( 'NONE', *, *, #111520, .F. ) ;
#30690=AXIS2_PLACEMENT_3D ( 'NONE', #113288, #24863, #45928 ) ;
#30750=DIRECTION ( 'NONE',  ( 0.000000000000000000, 0.000000000000000000, 1.000000000000000000 ) ) ;
#30842=LINE ( 'NONE', #67024, #57751 ) ;
#31120=SHAPE_REPRESENTATION_RELATIONSHIP ( 'NONE' , 'NONE' ,  #104156, #50002 ) ;
#31818=FILL_AREA_STYLE_COLOUR ( '', #35376 ) ;
#32122=DIRECTION ( 'NONE',  ( 1.000000000000000000, 0.000000000000000000, -0.000000000000000000 ) ) ;
#32465=EDGE_CURVE ( 'NONE', #65533, #27038, #91187, .T. ) ;
#33321=CIRCLE ( 'NONE', #81956, 6.499999999999999112 ) ;
#33326=CARTESIAN_POINT ( 'NONE',  ( 0.000000000000000000, 0.000000000000000000, -10.00000000000000000 ) ) ;
#33443=ORIENTED_EDGE ( 'NONE', *, *, #42088, .T. ) ;
#34006=DIRECTION ( 'NONE',  ( 1.000000000000000000, 0.000000000000000000, 0.000000000000000000 ) ) ;
#34052=ORIENTED_EDGE ( 'NONE', *, *, #6967, .F. ) ;
#34189=ORIENTED_EDGE ( 'NONE', *, *, #131576, .T. ) ;
#35152=VECTOR ( 'NONE', #82703, 1000.000000000000000 ) ;
#35205=EDGE_CURVE ( 'NONE', #133079, #103220, #61514, .T. ) ;
#35241=CARTESIAN_POINT ( 'NONE',  ( 1.179999999999999716, 6.391994993740215847, 10.00000000000000000 ) ) ;
#35376=COLOUR_RGB ( '', 0.66274510, 0.83137255, 0.94901961) ;
#35420=VERTEX_POINT ( 'NONE', #124244 ) ;
#35861=EDGE_CURVE ( 'NONE', #27927, #26527, #70570, .T. ) ;
#36358=DIRECTION ( 'NONE',  ( -0.000000000000000000, -0.000000000000000000, -1.000000000000000000 ) ) ;
#36665=EDGE_CURVE ( 'NONE', #5945, #66770, #30842, .T. ) ;
#36749=ORIENTED_EDGE ( 'NONE', *, *, #104011, .F. ) ;
#36835=AXIS2_PLACEMENT_3D ( 'NONE', #33326, #77528, #34006 ) ;
#37363=PRODUCT_CONTEXT ( 'NONE', #67989, 'mechanical' ) ;
#37505=DIRECTION ( 'NONE',  ( -0.000000000000000000, 0.000000000000000000, 1.000000000000000000 ) ) ;
#37521=EDGE_CURVE ( 'NONE', #44877, #5945, #84679, .T. ) ;
#38305=DIRECTION ( 'NONE',  ( -1.084202172485504434E-16, 1.000000000000000000, -0.000000000000000000 ) ) ;
#38605=PRODUCT_DEFINITION_CONTEXT ( 'detailed design', #50377, 'design' ) ;
#38800=DIRECTION ( 'NONE',  ( 1.000000000000000000, 0.000000000000000000, 0.000000000000000000 ) ) ;
#41082=EDGE_LOOP ( 'NONE', ( #36749, #96949 ) ) ;
#41163=CARTESIAN_POINT ( 'NONE',  ( 1.179999999999999272, 10.00000000000000178, 6.750000000000000888 ) ) ;
#41309=VERTEX_POINT ( 'NONE', #115046 ) ;
#41832=DIRECTION ( 'NONE',  ( 0.000000000000000000, 0.000000000000000000, 1.000000000000000000 ) ) ;
#41937=CYLINDRICAL_SURFACE ( 'NONE', #17661, 6.499999999999999112 ) ;
#42088=EDGE_CURVE ( 'NONE', #103220, #19931, #33321, .T. ) ;
#42357=VERTEX_POINT ( 'NONE', #120408 ) ;
#42401=VECTOR ( 'NONE', #100609, 1000.000000000000000 ) ;
#42845=DIRECTION ( 'NONE',  ( 1.192622389734054877E-16, -1.000000000000000000, 0.000000000000000000 ) ) ;
#43333=LINE ( 'NONE', #131771, #110081 ) ;
#43412=FILL_AREA_STYLE ('',( #31818 ) ) ;
#43425=PLANE ( 'NONE',  #53193 ) ;
#43685=CARTESIAN_POINT ( 'NONE',  ( 0.000000000000000000, 0.000000000000000000, 6.750000000000000888 ) ) ;
#44460=FACE_BOUND ( 'NONE', #106387, .T. ) ;
#44511=ORIENTED_EDGE ( 'NONE', *, *, #37521, .T. ) ;
#44598=STYLED_ITEM ( 'NONE', ( #67319 ), #50002 ) ;
#44689=CARTESIAN_POINT ( 'NONE',  ( 0.000000000000000000, 0.000000000000000000, 10.00000000000000000 ) ) ;
#44753=MANIFOLD_SOLID_BREP ( 'Cut-Extrude1', #4621 ) ;
#44877=VERTEX_POINT ( 'NONE', #103711 ) ;
#45127=PRESENTATION_STYLE_ASSIGNMENT (( #78435 ) ) ;
#45387=CARTESIAN_POINT ( 'NONE',  ( 0.000000000000000000, 0.000000000000000000, 10.00000000000000000 ) ) ;
#45762=DIRECTION ( 'NONE',  ( -1.000000000000000000, -1.192622389734054877E-16, 0.000000000000000000 ) ) ;
#45928=DIRECTION ( 'NONE',  ( 1.192622389734054877E-16, -1.000000000000000000, 0.000000000000000000 ) ) ;
#47438=STYLED_ITEM ( 'NONE', ( #45127 ), #44753 ) ;
#47472=DIRECTION ( 'NONE',  ( -0.000000000000000000, -0.000000000000000000, -1.000000000000000000 ) ) ;
#47547=DIRECTION ( 'NONE',  ( 0.000000000000000000, 0.000000000000000000, 1.000000000000000000 ) ) ;
#47807=EDGE_CURVE ( 'NONE', #15280, #66770, #136047, .T. ) ;
#48440=CARTESIAN_POINT ( 'NONE',  ( -1.180000000000000382, 6.391994993740215847, 6.750000000000000888 ) ) ;
#49056=ORIENTED_EDGE ( 'NONE', *, *, #20723, .T. ) ;
#49756=CIRCLE ( 'NONE', #126116, 9.119999999999999218 ) ;
#49776=VECTOR ( 'NONE', #102701, 1000.000000000000000 ) ;
#49980=DIRECTION ( 'NONE',  ( 1.000000000000000000, 1.084202172485504681E-16, 0.000000000000000000 ) ) ;
#50002=ADVANCED_BREP_SHAPE_REPRESENTATION ( '', ( #44753, #127880 ), #118637 ) ;
#50377=APPLICATION_CONTEXT ( 'automotive_design' ) ;
#50522=ORIENTED_EDGE ( 'NONE', *, *, #97640, .T. ) ;
#50548=ORIENTED_EDGE ( 'NONE', *, *, #79876, .T. ) ;
#50968=VERTEX_POINT ( 'NONE', #60509 ) ;
#51667=EDGE_LOOP ( 'NONE', ( #119281, #99608, #110975, #128830 ) ) ;
#51754=CIRCLE ( 'NONE', #24003, 9.119999999999999218 ) ;
#51841=ORIENTED_EDGE ( 'NONE', *, *, #3693, .T. ) ;
#52159=ORIENTED_EDGE ( 'NONE', *, *, #88105, .T. ) ;
#52315=ADVANCED_FACE ( 'NONE', ( #132205 ), #109712, .T. ) ;
#52464=DIRECTION ( 'NONE',  ( 1.000000000000000000, 0.000000000000000000, -0.000000000000000000 ) ) ;
#52502=ADVANCED_FACE ( 'NONE', ( #195 ), #100275, .F. ) ;
#52708=EDGE_LOOP ( 'NONE', ( #65188, #95186, #128986, #59597 ) ) ;
#52774=DIRECTION ( 'NONE',  ( -0.000000000000000000, -0.000000000000000000, -1.000000000000000000 ) ) ;
#53193=AXIS2_PLACEMENT_3D ( 'NONE', #54334, #76796, #21673 ) ;
#53195=DIRECTION ( 'NONE',  ( 1.000000000000000000, 0.000000000000000000, 0.000000000000000000 ) ) ;
#53581=( NAMED_UNIT ( * ) PLANE_ANGLE_UNIT ( ) SI_UNIT ( $, .RADIAN. ) );
#54279=EDGE_CURVE ( 'NONE', #44877, #15280, #9869, .T. ) ;
#54334=CARTESIAN_POINT ( 'NONE',  ( 0.000000000000000000, 0.000000000000000000, 6.750000000000000888 ) ) ;
#54353=COLOUR_RGB ( '', 0.66274510, 0.83137255, 0.94901961) ;
#54541=CARTESIAN_POINT ( 'NONE',  ( 1.180000000000000826, -6.391994993740215847, 6.750000000000000888 ) ) ;
#54957=VECTOR ( 'NONE', #57864, 1000.000000000000000 ) ;
#55016=SURFACE_STYLE_USAGE ( .BOTH. , #87625 ) ;
#55019=ADVANCED_FACE ( 'NONE', ( #133463 ), #67514, .F. ) ;
#55623=ORIENTED_EDGE ( 'NONE', *, *, #88105, .F. ) ;
#56650=ORIENTED_EDGE ( 'NONE', *, *, #47807, .T. ) ;
#56688=EDGE_CURVE ( 'NONE', #98793, #22459, #99327, .T. ) ;
#56752=CARTESIAN_POINT ( 'NONE',  ( -1.180000000000000160, 9.043340090917734386, 10.00000000000000000 ) ) ;
#56974=DIRECTION ( 'NONE',  ( 1.000000000000000000, 0.000000000000000000, -0.000000000000000000 ) ) ;
#57751=VECTOR ( 'NONE', #11899, 1000.000000000000000 ) ;
#57864=DIRECTION ( 'NONE',  ( 1.192622389734054877E-16, -1.000000000000000000, 0.000000000000000000 ) ) ;
#58489=ORIENTED_EDGE ( 'NONE', *, *, #54279, .T. ) ;
#58531=LINE ( 'NONE', #2640, #49776 ) ;
#58876=LINE ( 'NONE', #101591, #3582 ) ;
#58995=DIRECTION ( 'NONE',  ( 1.000000000000000000, 0.000000000000000000, 0.000000000000000000 ) ) ;
#59080=DIRECTION ( 'NONE',  ( -0.000000000000000000, -0.000000000000000000, -1.000000000000000000 ) ) ;
#59158=ORIENTED_EDGE ( 'NONE', *, *, #13502, .F. ) ;
#59386=CARTESIAN_POINT ( 'NONE',  ( -1.179999999999998384, -9.043340090917736163, 10.00000000000000000 ) ) ;
#59597=ORIENTED_EDGE ( 'NONE', *, *, #22168, .F. ) ;
#59666=FACE_OUTER_BOUND ( 'NONE', #68570, .T. ) ;
#59768=FACE_OUTER_BOUND ( 'NONE', #137908, .T. ) ;
#59885=ORIENTED_EDGE ( 'NONE', *, *, #102476, .F. ) ;
#60509=CARTESIAN_POINT ( 'NONE',  ( -6.499999999999999112, 0.000000000000000000, 10.00000000000000000 ) ) ;
#60877=PRODUCT_DEFINITION_SHAPE ( 'NONE', 'NONE',  #91726 ) ;
#61130=CARTESIAN_POINT ( 'NONE',  ( 9.119999999999999218, 1.116877880822386018E-15, -10.00000000000000000 ) ) ;
#61159=ORIENTED_EDGE ( 'NONE', *, *, #97640, .F. ) ;
#61514=LINE ( 'NONE', #124591, #24645 ) ;
#61747=ORIENTED_EDGE ( 'NONE', *, *, #114502, .F. ) ;
#61800=ORIENTED_EDGE ( 'NONE', *, *, #126753, .T. ) ;
#62166=AXIS2_PLACEMENT_3D ( 'NONE', #129763, #70625, #82205 ) ;
#62812=VERTEX_POINT ( 'NONE', #93135 ) ;
#63394=CARTESIAN_POINT ( 'NONE',  ( 0.000000000000000000, 0.000000000000000000, 10.00000000000000000 ) ) ;
#63485=VECTOR ( 'NONE', #82537, 1000.000000000000000 ) ;
#63958=CARTESIAN_POINT ( 'NONE',  ( 1.180000000000001270, -9.043340090917736163, 6.750000000000000888 ) ) ;
#64441=( LENGTH_UNIT ( ) NAMED_UNIT ( * ) SI_UNIT ( .MILLI., .METRE. ) );
#65188=ORIENTED_EDGE ( 'NONE', *, *, #66583, .F. ) ;
#65533=VERTEX_POINT ( 'NONE', #102000 ) ;
#65871=EDGE_LOOP ( 'NONE', ( #112634, #34189, #30147, #17924 ) ) ;
#66175=ORIENTED_EDGE ( 'NONE', *, *, #3693, .F. ) ;
#66548=CARTESIAN_POINT ( 'NONE',  ( -1.180000000000000604, 10.00000000000000178, 6.750000000000000888 ) ) ;
#66577=AXIS2_PLACEMENT_3D ( 'NONE', #44689, #47547, #56974 ) ;
#66583=EDGE_CURVE ( 'NONE', #65533, #41309, #102025, .T. ) ;
#66770=VERTEX_POINT ( 'NONE', #83876 ) ;
#67024=CARTESIAN_POINT ( 'NONE',  ( 1.179999999999998828, 9.043340090917734386, 10.00000000000000000 ) ) ;
#67149=VECTOR ( 'NONE', #121988, 1000.000000000000000 ) ;
#67319=PRESENTATION_STYLE_ASSIGNMENT (( #55016 ) ) ;
#67514=PLANE ( 'NONE',  #11735 ) ;
#67645=PLANE ( 'NONE',  #21456 ) ;
#67731=DIRECTION ( 'NONE',  ( 0.000000000000000000, 0.000000000000000000, 1.000000000000000000 ) ) ;
#67989=APPLICATION_CONTEXT ( 'automotive_design' ) ;
#68389=ADVANCED_FACE ( 'NONE', ( #59666 ), #103816, .F. ) ;
#68570=EDGE_LOOP ( 'NONE', ( #128192, #129792, #104821, #59885 ) ) ;
#68715=CARTESIAN_POINT ( 'NONE',  ( -1.180000000000000604, 9.043340090917736163, 10.00000000000000000 ) ) ;
#68732=CARTESIAN_POINT ( 'NONE',  ( -1.180000000000000604, 10.00000000000000178, 10.00000000000000000 ) ) ;
#68998=DIRECTION ( 'NONE',  ( 0.000000000000000000, 0.000000000000000000, 1.000000000000000000 ) ) ;
#69112=VECTOR ( 'NONE', #8492, 1000.000000000000000 ) ;
#69823=CARTESIAN_POINT ( 'NONE',  ( 0.000000000000000000, 0.000000000000000000, 10.00000000000000000 ) ) ;
#70570=LINE ( 'NONE', #114714, #131936 ) ;
#70625=DIRECTION ( 'NONE',  ( -0.000000000000000000, 0.000000000000000000, 1.000000000000000000 ) ) ;
#70740=DIRECTION ( 'NONE',  ( 0.000000000000000000, 0.000000000000000000, 1.000000000000000000 ) ) ;
#71125=LINE ( 'NONE', #15960, #35152 ) ;
#71604=ORIENTED_EDGE ( 'NONE', *, *, #22168, .T. ) ;
#71969=VECTOR ( 'NONE', #42845, 1000.000000000000000 ) ;
#72340=CARTESIAN_POINT ( 'NONE',  ( 0.000000000000000000, 0.000000000000000000, 10.00000000000000000 ) ) ;
#72691=EDGE_LOOP ( 'NONE', ( #2858, #51841, #104076, #8041, #61747, #29700 ) ) ;
#73291=CARTESIAN_POINT ( 'NONE',  ( 0.000000000000000000, 0.000000000000000000, 6.750000000000000888 ) ) ;
#74784=ORIENTED_EDGE ( 'NONE', *, *, #6981, .F. ) ;
#75090=UNCERTAINTY_MEASURE_WITH_UNIT (LENGTH_MEASURE( 1.000000000000000082E-05 ), #64441, 'distance_accuracy_value', 'NONE');
#75186=ORIENTED_EDGE ( 'NONE', *, *, #111520, .T. ) ;
#75969=ADVANCED_FACE ( 'NONE', ( #59768 ), #106067, .T. ) ;
#76220=ORIENTED_EDGE ( 'NONE', *, *, #141162, .F. ) ;
#76796=DIRECTION ( 'NONE',  ( -0.000000000000000000, 0.000000000000000000, 1.000000000000000000 ) ) ;
#77528=DIRECTION ( 'NONE',  ( 0.000000000000000000, 0.000000000000000000, 1.000000000000000000 ) ) ;
#78007=DIRECTION ( 'NONE',  ( 0.000000000000000000, 0.000000000000000000, 1.000000000000000000 ) ) ;
#78021=ADVANCED_FACE ( 'NONE', ( #87926, #44460 ), #67645, .F. ) ;
#78147=CARTESIAN_POINT ( 'NONE',  ( 1.179999999999999272, 10.00000000000000178, 6.750000000000000888 ) ) ;
#78435=SURFACE_STYLE_USAGE ( .BOTH. , #142961 ) ;
#78697=DIRECTION ( 'NONE',  ( 1.000000000000000000, 0.000000000000000000, 0.000000000000000000 ) ) ;
#78949=VERTEX_POINT ( 'NONE', #68715 ) ;
#79181=( LENGTH_UNIT ( ) NAMED_UNIT ( * ) SI_UNIT ( .MILLI., .METRE. ) );
#79876=EDGE_CURVE ( 'NONE', #5945, #27927, #134894, .T. ) ;
#79904=CARTESIAN_POINT ( 'NONE',  ( 0.000000000000000000, 0.000000000000000000, -10.00000000000000000 ) ) ;
#81522=VERTEX_POINT ( 'NONE', #59386 ) ;
#81530=EDGE_CURVE ( 'NONE', #103220, #131264, #115117, .T. ) ;
#81624=( GEOMETRIC_REPRESENTATION_CONTEXT ( 3 ) GLOBAL_UNCERTAINTY_ASSIGNED_CONTEXT ( ( #75090 ) ) GLOBAL_UNIT_ASSIGNED_CONTEXT ( ( #64441, #108624, #130433 ) ) REPRESENTATION_CONTEXT ( 'NONE', 'WORKASPACE' ) );
#81777=CYLINDRICAL_SURFACE ( 'NONE', #133458, 9.119999999999999218 ) ;
#81851=CIRCLE ( 'NONE', #86388, 6.499999999999999112 ) ;
#81956=AXIS2_PLACEMENT_3D ( 'NONE', #14719, #115414, #58995 ) ;
#82205=DIRECTION ( 'NONE',  ( 1.000000000000000000, 0.000000000000000000, 0.000000000000000000 ) ) ;
#82344=CIRCLE ( 'NONE', #105395, 6.499999999999999112 ) ;
#82537=DIRECTION ( 'NONE',  ( -0.000000000000000000, -0.000000000000000000, -1.000000000000000000 ) ) ;
#82703=DIRECTION ( 'NONE',  ( -1.084202172485504434E-16, 1.000000000000000000, -0.000000000000000000 ) ) ;
#82936=DIRECTION ( 'NONE',  ( -1.000000000000000000, 0.000000000000000000, 0.000000000000000000 ) ) ;
#83185=VECTOR ( 'NONE', #125905, 1000.000000000000000 ) ;
#83829=UNCERTAINTY_MEASURE_WITH_UNIT (LENGTH_MEASURE( 1.000000000000000082E-05 ), #131855, 'distance_accuracy_value', 'NONE');
#83876=CARTESIAN_POINT ( 'NONE',  ( 1.179999999999999272, 9.043340090917736163, 10.00000000000000000 ) ) ;
#84679=LINE ( 'NONE', #41163, #69112 ) ;
#85353=CARTESIAN_POINT ( 'NONE',  ( -1.180000000000000604, 9.043340090917736163, 6.750000000000000888 ) ) ;
#85843=AXIS2_PLACEMENT_3D ( 'NONE', #17165, #37505, #126610 ) ;
#86081=VECTOR ( 'NONE', #78007, 1000.000000000000000 ) ;
#86227=AXIS2_PLACEMENT_3D ( 'NONE', #131123, #110753, #99917 ) ;
#86388=AXIS2_PLACEMENT_3D ( 'NONE', #43685, #132143, #101624 ) ;
#86449=CARTESIAN_POINT ( 'NONE',  ( -1.179999999999998606, -6.391994993740215847, 10.00000000000000000 ) ) ;
#86866=DIRECTION ( 'NONE',  ( -1.000000000000000000, 0.000000000000000000, 0.000000000000000000 ) ) ;
#87625=SURFACE_SIDE_STYLE ('',( #110771 ) ) ;
#87666=AXIS2_PLACEMENT_3D ( 'NONE', #99629, #91630, #111214 ) ;
#87899=DIRECTION ( 'NONE',  ( -0.000000000000000000, -0.000000000000000000, -1.000000000000000000 ) ) ;
#87926=FACE_OUTER_BOUND ( 'NONE', #41082, .T. ) ;
#88105=EDGE_CURVE ( 'NONE', #62812, #22459, #58531, .T. ) ;
#88296=FACE_OUTER_BOUND ( 'NONE', #8111, .T. ) ;
#88894=CARTESIAN_POINT ( 'NONE',  ( 1.179999999999999272, 6.391994993740214959, 10.00000000000000000 ) ) ;
#89033=DIRECTION ( 'NONE',  ( 1.000000000000000000, 1.084202172485504681E-16, 0.000000000000000000 ) ) ;
#89492=LINE ( 'NONE', #123592, #110955 ) ;
#89564=DIRECTION ( 'NONE',  ( 0.000000000000000000, 0.000000000000000000, 1.000000000000000000 ) ) ;
#90104=CARTESIAN_POINT ( 'NONE',  ( -6.499999999999999112, 0.000000000000000000, 10.00000000000000000 ) ) ;
#90440=ADVANCED_FACE ( 'NONE', ( #112204 ), #12850, .F. ) ;
#90521=CIRCLE ( 'NONE', #85843, 9.119999999999999218 ) ;
#90844=EDGE_CURVE ( 'NONE', #99639, #50968, #82344, .T. ) ;
#91187=LINE ( 'NONE', #135402, #3100 ) ;
#91630=DIRECTION ( 'NONE',  ( 0.000000000000000000, 0.000000000000000000, 1.000000000000000000 ) ) ;
#91665=ADVANCED_FACE ( 'NONE', ( #28074 ), #81777, .T. ) ;
#91673=AXIS2_PLACEMENT_3D ( 'NONE', #79904, #68998, #124781 ) ;
#91726=PRODUCT_DEFINITION ( 'UNKNOWN', '', #111928, #38605 ) ;
#92735=CARTESIAN_POINT ( 'NONE',  ( 1.179999999999999272, 10.00000000000000178, 6.750000000000000888 ) ) ;
#93135=CARTESIAN_POINT ( 'NONE',  ( -9.119999999999999218, 0.000000000000000000, 10.00000000000000000 ) ) ;
#93306=VECTOR ( 'NONE', #87899, 1000.000000000000000 ) ;
#93327=DIRECTION ( 'NONE',  ( -1.000000000000000000, 0.000000000000000000, 0.000000000000000000 ) ) ;
#94163=DIRECTION ( 'NONE',  ( -1.084202172485504681E-16, 1.000000000000000000, 0.000000000000000000 ) ) ;
#94497=CARTESIAN_POINT ( 'NONE',  ( 0.000000000000000000, 0.000000000000000000, 10.00000000000000000 ) ) ;
#94817=AXIS2_PLACEMENT_3D ( 'NONE', #135808, #67731, #101744 ) ;
#95186=ORIENTED_EDGE ( 'NONE', *, *, #32465, .T. ) ;
#95710=ORIENTED_EDGE ( 'NONE', *, *, #81530, .F. ) ;
#96393=PLANE ( 'NONE',  #62166 ) ;
#96413=DIRECTION ( 'NONE',  ( 1.000000000000000000, 0.000000000000000000, 0.000000000000000000 ) ) ;
#96675=ORIENTED_EDGE ( 'NONE', *, *, #117021, .T. ) ;
#96949=ORIENTED_EDGE ( 'NONE', *, *, #56688, .F. ) ;
#96962=CARTESIAN_POINT ( 'NONE',  ( 1.180000000000000826, -6.391994993740215847, 10.00000000000000000 ) ) ;
#97509=AXIS2_PLACEMENT_3D ( 'NONE', #140423, #41832, #7749 ) ;
#97640=EDGE_CURVE ( 'NONE', #18391, #98793, #122720, .T. ) ;
#97841=ORIENTED_EDGE ( 'NONE', *, *, #21081, .T. ) ;
#98732=( NAMED_UNIT ( * ) PLANE_ANGLE_UNIT ( ) SI_UNIT ( $, .RADIAN. ) );
#98793=VERTEX_POINT ( 'NONE', #61130 ) ;
#99182=( NAMED_UNIT ( * ) SI_UNIT ( $, .STERADIAN. ) SOLID_ANGLE_UNIT ( ) );
#99327=CIRCLE ( 'NONE', #36835, 9.119999999999999218 ) ;
#99526=DIRECTION ( 'NONE',  ( -0.000000000000000000, -0.000000000000000000, -1.000000000000000000 ) ) ;
#99608=ORIENTED_EDGE ( 'NONE', *, *, #81530, .T. ) ;
#99629=CARTESIAN_POINT ( 'NONE',  ( 0.000000000000000000, 0.000000000000000000, 10.00000000000000000 ) ) ;
#99639=VERTEX_POINT ( 'NONE', #114216 ) ;
#99883=DIRECTION ( 'NONE',  ( -1.084202172485504681E-16, 1.000000000000000000, 0.000000000000000000 ) ) ;
#99917=DIRECTION ( 'NONE',  ( 1.000000000000000000, 0.000000000000000000, 0.000000000000000000 ) ) ;
#100275=CYLINDRICAL_SURFACE ( 'NONE', #9142, 6.499999999999999112 ) ;
#100609=DIRECTION ( 'NONE',  ( 1.192622389734054877E-16, -1.000000000000000000, 0.000000000000000000 ) ) ;
#100773=CARTESIAN_POINT ( 'NONE',  ( -1.180000000000000604, 10.00000000000000178, 10.00000000000000000 ) ) ;
#101151=CIRCLE ( 'NONE', #10785, 9.119999999999999218 ) ;
#101188=ORIENTED_EDGE ( 'NONE', *, *, #133421, .F. ) ;
#101591=CARTESIAN_POINT ( 'NONE',  ( 6.499999999999999112, 7.960204194457794491E-16, 10.00000000000000000 ) ) ;
#101624=DIRECTION ( 'NONE',  ( 1.000000000000000000, 0.000000000000000000, 0.000000000000000000 ) ) ;
#101744=DIRECTION ( 'NONE',  ( 1.000000000000000000, 0.000000000000000000, 0.000000000000000000 ) ) ;
#101867=PLANE ( 'NONE',  #66577 ) ;
#102000=CARTESIAN_POINT ( 'NONE',  ( -1.179999999999998606, -6.391994993740215847, 6.750000000000000888 ) ) ;
#102025=LINE ( 'NONE', #66548, #42401 ) ;
#102476=EDGE_CURVE ( 'NONE', #78949, #27927, #111048, .T. ) ;
#102498=EDGE_CURVE ( 'NONE', #44877, #26527, #81851, .T. ) ;
#102701=DIRECTION ( 'NONE',  ( -0.000000000000000000, -0.000000000000000000, -1.000000000000000000 ) ) ;
#103220=VERTEX_POINT ( 'NONE', #96962 ) ;
#103711=CARTESIAN_POINT ( 'NONE',  ( 1.179999999999999716, 6.391994993740215847, 6.750000000000000888 ) ) ;
#103816=PLANE ( 'NONE',  #30690 ) ;
#104011=EDGE_CURVE ( 'NONE', #22459, #98793, #49756, .T. ) ;
#104076=ORIENTED_EDGE ( 'NONE', *, *, #13502, .T. ) ;
#104156=SHAPE_REPRESENTATION ( '1.4 Collar', ( #127880 ), #118637 ) ;
#104262=ADVANCED_FACE ( 'NONE', ( #126111 ), #123973, .F. ) ;
#104821=ORIENTED_EDGE ( 'NONE', *, *, #35861, .F. ) ;
#105395=AXIS2_PLACEMENT_3D ( 'NONE', #45387, #89564, #78697 ) ;
#106067=CYLINDRICAL_SURFACE ( 'NONE', #2483, 9.119999999999999218 ) ;
#106258=CIRCLE ( 'NONE', #127187, 6.499999999999999112 ) ;
#106387=EDGE_LOOP ( 'NONE', ( #116890, #97841 ) ) ;
#106577=DIRECTION ( 'NONE',  ( -0.000000000000000000, 0.000000000000000000, 1.000000000000000000 ) ) ;
#106623=CARTESIAN_POINT ( 'NONE',  ( 0.000000000000000000, 0.000000000000000000, -10.00000000000000000 ) ) ;
#106729=VERTEX_POINT ( 'NONE', #63958 ) ;
#106804=DIRECTION ( 'NONE',  ( 0.000000000000000000, 0.000000000000000000, 1.000000000000000000 ) ) ;
#108561=EDGE_LOOP ( 'NONE', ( #33443, #3077, #74784, #30594, #96675, #2069, #23490, #95710 ) ) ;
#108624=( NAMED_UNIT ( * ) PLANE_ANGLE_UNIT ( ) SI_UNIT ( $, .RADIAN. ) );
#108710=AXIS2_PLACEMENT_3D ( 'NONE', #63394, #30750, #52464 ) ;
#109712=PLANE ( 'NONE',  #108710 ) ;
#110081=VECTOR ( 'NONE', #10661, 1000.000000000000000 ) ;
#110197=LINE ( 'NONE', #100773, #71969 ) ;
#110753=DIRECTION ( 'NONE',  ( -0.000000000000000000, 0.000000000000000000, 1.000000000000000000 ) ) ;
#110771=SURFACE_STYLE_FILL_AREA ( #43412 ) ;
#110955=VECTOR ( 'NONE', #47472, 1000.000000000000000 ) ;
#110975=ORIENTED_EDGE ( 'NONE', *, *, #131576, .F. ) ;
#110978=CARTESIAN_POINT ( 'NONE',  ( 9.119999999999999218, 1.116877880822386018E-15, 10.00000000000000000 ) ) ;
#111022=FILL_AREA_STYLE ('',( #123389 ) ) ;
#111048=LINE ( 'NONE', #56752, #93306 ) ;
#111125=DIRECTION ( 'NONE',  ( -0.000000000000000000, -0.000000000000000000, -1.000000000000000000 ) ) ;
#111172=CIRCLE ( 'NONE', #118087, 6.499999999999999112 ) ;
#111214=DIRECTION ( 'NONE',  ( 1.000000000000000000, 0.000000000000000000, 0.000000000000000000 ) ) ;
#111453=CARTESIAN_POINT ( 'NONE',  ( 0.000000000000000000, 0.000000000000000000, 10.00000000000000000 ) ) ;
#111488=DIRECTION ( 'NONE',  ( 1.000000000000000000, 0.000000000000000000, 0.000000000000000000 ) ) ;
#111520=EDGE_CURVE ( 'NONE', #50968, #35420, #135089, .T. ) ;
#111928=PRODUCT_DEFINITION_FORMATION_WITH_SPECIFIED_SOURCE ( 'ANY', '', #118763, .NOT_KNOWN. ) ;
#112204=FACE_OUTER_BOUND ( 'NONE', #51667, .T. ) ;
#112634=ORIENTED_EDGE ( 'NONE', *, *, #141162, .T. ) ;
#113263=CARTESIAN_POINT ( 'NONE',  ( 9.119999999999999218, 1.116877880822386018E-15, 10.00000000000000000 ) ) ;
#113268=DIRECTION ( 'NONE',  ( -1.000000000000000000, 0.000000000000000000, 0.000000000000000000 ) ) ;
#113288=CARTESIAN_POINT ( 'NONE',  ( -1.180000000000000604, 10.00000000000000178, 6.750000000000000888 ) ) ;
#113716=CARTESIAN_POINT ( 'NONE',  ( 6.499999999999999112, 7.960204194457794491E-16, 10.00000000000000000 ) ) ;
#114216=CARTESIAN_POINT ( 'NONE',  ( -1.180000000000000382, 6.391994993740215847, 10.00000000000000000 ) ) ;
#114502=EDGE_CURVE ( 'NONE', #19931, #15280, #136543, .T. ) ;
#114530=MECHANICAL_DESIGN_GEOMETRIC_PRESENTATION_REPRESENTATION('',(#47438),#24212);
#114714=CARTESIAN_POINT ( 'NONE',  ( -1.180000000000000604, 10.00000000000000178, 6.750000000000000888 ) ) ;
#115046=CARTESIAN_POINT ( 'NONE',  ( -1.179999999999998384, -9.043340090917736163, 6.750000000000000888 ) ) ;
#115117=LINE ( 'NONE', #15788, #63485 ) ;
#115338=DIRECTION ( 'NONE',  ( 0.000000000000000000, 0.000000000000000000, 1.000000000000000000 ) ) ;
#115414=DIRECTION ( 'NONE',  ( 0.000000000000000000, 0.000000000000000000, 1.000000000000000000 ) ) ;
#115616=ORIENTED_EDGE ( 'NONE', *, *, #35861, .T. ) ;
#116033=CIRCLE ( 'NONE', #97509, 6.499999999999999112 ) ;
#116890=ORIENTED_EDGE ( 'NONE', *, *, #6981, .T. ) ;
#117021=EDGE_CURVE ( 'NONE', #50968, #27038, #116033, .T. ) ;
#117623=DIRECTION ( 'NONE',  ( 0.000000000000000000, 0.000000000000000000, 1.000000000000000000 ) ) ;
#118087=AXIS2_PLACEMENT_3D ( 'NONE', #73291, #106577, #96413 ) ;
#118291=ORIENTED_EDGE ( 'NONE', *, *, #102498, .F. ) ;
#118637=( GEOMETRIC_REPRESENTATION_CONTEXT ( 3 ) GLOBAL_UNCERTAINTY_ASSIGNED_CONTEXT ( ( #83829 ) ) GLOBAL_UNIT_ASSIGNED_CONTEXT ( ( #131855, #53581, #99182 ) ) REPRESENTATION_CONTEXT ( 'NONE', 'WORKASPACE' ) );
#118763=PRODUCT ( '1.4 Collar', '1.4 Collar', '', ( #37363 ) ) ;
#119281=ORIENTED_EDGE ( 'NONE', *, *, #35205, .T. ) ;
#120408=CARTESIAN_POINT ( 'NONE',  ( 6.499999999999999112, 7.960204194457794491E-16, -10.00000000000000000 ) ) ;
#121988=DIRECTION ( 'NONE',  ( -0.000000000000000000, -0.000000000000000000, -1.000000000000000000 ) ) ;
#122505=CARTESIAN_POINT ( 'NONE',  ( -9.119999999999999218, 0.000000000000000000, -10.00000000000000000 ) ) ;
#122720=LINE ( 'NONE', #113263, #67149 ) ;
#123389=FILL_AREA_STYLE_COLOUR ( '', #54353 ) ;
#123592=CARTESIAN_POINT ( 'NONE',  ( 1.180000000000000826, -9.043340090917734386, 10.00000000000000000 ) ) ;
#123683=ORIENTED_EDGE ( 'NONE', *, *, #117021, .F. ) ;
#123808=DIRECTION ( 'NONE',  ( 0.000000000000000000, 0.000000000000000000, 1.000000000000000000 ) ) ;
#123973=PLANE ( 'NONE',  #17232 ) ;
#124244=CARTESIAN_POINT ( 'NONE',  ( -6.499999999999999112, 0.000000000000000000, -10.00000000000000000 ) ) ;
#124405=CIRCLE ( 'NONE', #128959, 9.119999999999999218 ) ;
#124591=CARTESIAN_POINT ( 'NONE',  ( 1.179999999999999272, 10.00000000000000178, 10.00000000000000000 ) ) ;
#124620=CARTESIAN_POINT ( 'NONE',  ( 1.180000000000001270, -9.043340090917736163, 10.00000000000000000 ) ) ;
#124631=UNCERTAINTY_MEASURE_WITH_UNIT (LENGTH_MEASURE( 1.000000000000000082E-05 ), #79181, 'distance_accuracy_value', 'NONE');
#124781=DIRECTION ( 'NONE',  ( 1.000000000000000000, 0.000000000000000000, 0.000000000000000000 ) ) ;
#125018=VECTOR ( 'NONE', #115338, 1000.000000000000000 ) ;
#125162=ORIENTED_EDGE ( 'NONE', *, *, #21081, .F. ) ;
#125716=ADVANCED_FACE ( 'NONE', ( #26369 ), #96393, .T. ) ;
#125905=DIRECTION ( 'NONE',  ( -1.084202172485504434E-16, 1.000000000000000000, -0.000000000000000000 ) ) ;
#126111=FACE_OUTER_BOUND ( 'NONE', #28973, .T. ) ;
#126116=AXIS2_PLACEMENT_3D ( 'NONE', #106623, #8715, #130570 ) ;
#126583=CARTESIAN_POINT ( 'NONE',  ( 1.179999999999999272, 10.00000000000000178, 10.00000000000000000 ) ) ;
#126610=DIRECTION ( 'NONE',  ( 1.000000000000000000, 0.000000000000000000, 0.000000000000000000 ) ) ;
#126753=EDGE_CURVE ( 'NONE', #133079, #106729, #89492, .T. ) ;
#127187=AXIS2_PLACEMENT_3D ( 'NONE', #142975, #117623, #18309 ) ;
#127205=SHAPE_DEFINITION_REPRESENTATION ( #60877, #104156 ) ;
#127880=AXIS2_PLACEMENT_3D ( 'NONE', #8925, #141658, #53195 ) ;
#127884=EDGE_CURVE ( 'NONE', #65533, #131264, #111172, .T. ) ;
#127889=CARTESIAN_POINT ( 'NONE',  ( 0.000000000000000000, 0.000000000000000000, 10.00000000000000000 ) ) ;
#128192=ORIENTED_EDGE ( 'NONE', *, *, #22469, .T. ) ;
#128603=EDGE_LOOP ( 'NONE', ( #140916, #49056, #14539, #10396, #123683, #130753 ) ) ;
#128830=ORIENTED_EDGE ( 'NONE', *, *, #126753, .F. ) ;
#128959=AXIS2_PLACEMENT_3D ( 'NONE', #25184, #23021, #111488 ) ;
#128986=ORIENTED_EDGE ( 'NONE', *, *, #135348, .T. ) ;
#129763=CARTESIAN_POINT ( 'NONE',  ( 0.000000000000000000, 0.000000000000000000, 6.750000000000000888 ) ) ;
#129792=ORIENTED_EDGE ( 'NONE', *, *, #133421, .T. ) ;
#130433=( NAMED_UNIT ( * ) SI_UNIT ( $, .STERADIAN. ) SOLID_ANGLE_UNIT ( ) );
#130570=DIRECTION ( 'NONE',  ( 1.000000000000000000, 0.000000000000000000, 0.000000000000000000 ) ) ;
#130753=ORIENTED_EDGE ( 'NONE', *, *, #90844, .F. ) ;
#131123=CARTESIAN_POINT ( 'NONE',  ( 0.000000000000000000, 0.000000000000000000, 6.750000000000000888 ) ) ;
#131264=VERTEX_POINT ( 'NONE', #54541 ) ;
#131576=EDGE_CURVE ( 'NONE', #106729, #131264, #71125, .T. ) ;
#131771=CARTESIAN_POINT ( 'NONE',  ( -1.179999999999999938, 6.391994993740214959, 10.00000000000000000 ) ) ;
#131855=( LENGTH_UNIT ( ) NAMED_UNIT ( * ) SI_UNIT ( .MILLI., .METRE. ) );
#131936=VECTOR ( 'NONE', #15387, 1000.000000000000000 ) ;
#132143=DIRECTION ( 'NONE',  ( -0.000000000000000000, 0.000000000000000000, 1.000000000000000000 ) ) ;
#132171=CARTESIAN_POINT ( 'NONE',  ( 0.000000000000000000, 0.000000000000000000, -10.00000000000000000 ) ) ;
#132205=FACE_OUTER_BOUND ( 'NONE', #72691, .T. ) ;
#133079=VERTEX_POINT ( 'NONE', #124620 ) ;
#133421=EDGE_CURVE ( 'NONE', #99639, #26527, #43333, .T. ) ;
#133458=AXIS2_PLACEMENT_3D ( 'NONE', #72340, #4836, #93327 ) ;
#133463=FACE_OUTER_BOUND ( 'NONE', #52708, .T. ) ;
#133619=ORIENTED_EDGE ( 'NONE', *, *, #56688, .T. ) ;
#134383=ADVANCED_FACE ( 'NONE', ( #88296 ), #41937, .F. ) ;
#134894=CIRCLE ( 'NONE', #86227, 9.119999999999999218 ) ;
#134981=( NAMED_UNIT ( * ) SI_UNIT ( $, .STERADIAN. ) SOLID_ANGLE_UNIT ( ) );
#135089=LINE ( 'NONE', #90104, #6232 ) ;
#135348=EDGE_CURVE ( 'NONE', #27038, #81522, #24481, .T. ) ;
#135402=CARTESIAN_POINT ( 'NONE',  ( -1.179999999999998161, -6.391994993740214959, 10.00000000000000000 ) ) ;
#135808=CARTESIAN_POINT ( 'NONE',  ( 0.000000000000000000, 0.000000000000000000, 10.00000000000000000 ) ) ;
#136047=LINE ( 'NONE', #126583, #83185 ) ;
#136543=CIRCLE ( 'NONE', #94817, 6.499999999999999112 ) ;
#136955=ORIENTED_EDGE ( 'NONE', *, *, #37521, .F. ) ;
#137908=EDGE_LOOP ( 'NONE', ( #61159, #66175, #61800, #76220, #71604, #16018, #52159, #3011 ) ) ;
#138751=ORIENTED_EDGE ( 'NONE', *, *, #102476, .T. ) ;
#140423=CARTESIAN_POINT ( 'NONE',  ( 0.000000000000000000, 0.000000000000000000, 10.00000000000000000 ) ) ;
#140916=ORIENTED_EDGE ( 'NONE', *, *, #22469, .F. ) ;
#141162=EDGE_CURVE ( 'NONE', #41309, #106729, #90521, .T. ) ;
#141658=DIRECTION ( 'NONE',  ( 0.000000000000000000, 0.000000000000000000, 1.000000000000000000 ) ) ;
#142303=ORIENTED_EDGE ( 'NONE', *, *, #36665, .T. ) ;
#142961=SURFACE_SIDE_STYLE ('',( #838 ) ) ;
#142975=CARTESIAN_POINT ( 'NONE',  ( 0.000000000000000000, 0.000000000000000000, -10.00000000000000000 ) ) ;
#143477=EDGE_LOOP ( 'NONE', ( #50548, #115616, #118291, #44511 ) ) ;
ENDSEC;
END-ISO-10303-21;
